ISO-10303-21;
HEADER;
/* Generated by software containing ST-Developer
 * from STEP Tools, Inc. (www.steptools.com) 
 */

FILE_DESCRIPTION(
/* description */ ('Pipe clamp stand with threaded column'),
/* implementation_level */ '2;1');

FILE_NAME(
/* name */ 'M8x40 clamp bolt.step',
/* time_stamp */ '2026-10-27T10:55:48-07:00',
/* author */ (''),
/* organization */ (''),
/* preprocessor_version */ 'ST-DEVELOPER v20.2',
/* originating_system */ 'Autodesk Translation Framework v15.17.0.0',
/* authorisation */ '');

FILE_SCHEMA (('AUTOMOTIVE_DESIGN { 1 0 10303 214 3 1 1 }'));
ENDSEC;

DATA;
#10=MECHANICAL_DESIGN_GEOMETRIC_PRESENTATION_REPRESENTATION('',(#764),#34433);
#198=CONICAL_SURFACE('',#9550,0.625,0.785398163397448);
#199=CONICAL_SURFACE('',#9554,0.635,0.785398163397449);
#200=CONICAL_SURFACE('',#9558,0.41,0.463647609000806);
#204=ORIENTED_CLOSED_SHELL('',*,#8792,.F.);
#206=BREP_WITH_VOIDS('Body1',#8793,(#204));
#712=SHAPE_REPRESENTATION_RELATIONSHIP('SRR','None',#34554,#734);
#734=ADVANCED_BREP_SHAPE_REPRESENTATION('',(#206),#34422);
#764=STYLED_ITEM('',(#34750),#206);
#843=FACE_BOUND('',#1958,.T.);
#844=FACE_BOUND('',#1966,.T.);
#990=PLANE('',#9534);
#991=PLANE('',#9535);
#992=PLANE('',#9536);
#993=PLANE('',#9537);
#994=PLANE('',#9538);
#995=PLANE('',#9539);
#996=PLANE('',#9540);
#997=PLANE('',#9541);
#998=PLANE('',#9542);
#999=PLANE('',#9547);
#1000=PLANE('',#9548);
#1001=PLANE('',#9556);
#1418=FACE_OUTER_BOUND('',#1949,.T.);
#1419=FACE_OUTER_BOUND('',#1950,.T.);
#1420=FACE_OUTER_BOUND('',#1951,.T.);
#1421=FACE_OUTER_BOUND('',#1952,.T.);
#1422=FACE_OUTER_BOUND('',#1953,.T.);
#1423=FACE_OUTER_BOUND('',#1954,.T.);
#1424=FACE_OUTER_BOUND('',#1955,.T.);
#1425=FACE_OUTER_BOUND('',#1956,.T.);
#1426=FACE_OUTER_BOUND('',#1957,.T.);
#1427=FACE_OUTER_BOUND('',#1959,.T.);
#1428=FACE_OUTER_BOUND('',#1960,.T.);
#1429=FACE_OUTER_BOUND('',#1961,.T.);
#1430=FACE_OUTER_BOUND('',#1962,.T.);
#1431=FACE_OUTER_BOUND('',#1963,.T.);
#1432=FACE_OUTER_BOUND('',#1964,.T.);
#1433=FACE_OUTER_BOUND('',#1965,.T.);
#1434=FACE_OUTER_BOUND('',#1967,.T.);
#1435=FACE_OUTER_BOUND('',#1968,.T.);
#1949=EDGE_LOOP('',(#7439,#7440,#7441,#7442));
#1950=EDGE_LOOP('',(#7443,#7444,#7445,#7446));
#1951=EDGE_LOOP('',(#7447,#7448,#7449,#7450));
#1952=EDGE_LOOP('',(#7451,#7452,#7453,#7454));
#1953=EDGE_LOOP('',(#7455,#7456,#7457,#7458));
#1954=EDGE_LOOP('',(#7459,#7460,#7461,#7462));
#1955=EDGE_LOOP('',(#7463,#7464,#7465,#7466,#7467,#7468));
#1956=EDGE_LOOP('',(#7469,#7470,#7471,#7472,#7473,#7474));
#1957=EDGE_LOOP('',(#7475));
#1958=EDGE_LOOP('',(#7476));
#1959=EDGE_LOOP('',(#7477,#7478,#7479,#7480));
#1960=EDGE_LOOP('',(#7481));
#1961=EDGE_LOOP('',(#7482));
#1962=EDGE_LOOP('',(#7483,#7484,#7485,#7486));
#1963=EDGE_LOOP('',(#7487,#7488,#7489,#7490));
#1964=EDGE_LOOP('',(#7491,#7492,#7493,#7494));
#1965=EDGE_LOOP('',(#7495));
#1966=EDGE_LOOP('',(#7496));
#1967=EDGE_LOOP('',(#7497,#7498,#7499,#7500));
#1968=EDGE_LOOP('',(#7501,#7502,#7503,#7504));
#2554=LINE('',#28748,#3171);
#2555=LINE('',#28750,#3172);
#2556=LINE('',#28752,#3173);
#2557=LINE('',#28753,#3174);
#2558=LINE('',#28756,#3175);
#2559=LINE('',#28758,#3176);
#2560=LINE('',#28759,#3177);
#2561=LINE('',#28762,#3178);
#2562=LINE('',#28764,#3179);
#2563=LINE('',#28765,#3180);
#2564=LINE('',#28768,#3181);
#2565=LINE('',#28770,#3182);
#2566=LINE('',#28771,#3183);
#2567=LINE('',#28774,#3184);
#2568=LINE('',#28776,#3185);
#2569=LINE('',#28777,#3186);
#2570=LINE('',#28779,#3187);
#2571=LINE('',#28780,#3188);
#2572=LINE('',#28790,#3189);
#2573=LINE('',#28799,#3190);
#2574=LINE('',#28803,#3191);
#2575=LINE('',#28807,#3192);
#2576=LINE('',#28814,#3193);
#2577=LINE('',#28816,#3194);
#3171=VECTOR('',#11187,1.);
#3172=VECTOR('',#11188,1.);
#3173=VECTOR('',#11189,1.);
#3174=VECTOR('',#11190,1.);
#3175=VECTOR('',#11193,1.);
#3176=VECTOR('',#11194,1.);
#3177=VECTOR('',#11195,1.);
#3178=VECTOR('',#11198,1.);
#3179=VECTOR('',#11199,1.);
#3180=VECTOR('',#11200,1.);
#3181=VECTOR('',#11203,1.);
#3182=VECTOR('',#11204,1.);
#3183=VECTOR('',#11205,1.);
#3184=VECTOR('',#11208,1.);
#3185=VECTOR('',#11209,1.);
#3186=VECTOR('',#11210,1.);
#3187=VECTOR('',#11213,1.);
#3188=VECTOR('',#11214,1.);
#3189=VECTOR('',#11227,0.4);
#3190=VECTOR('',#11240,0.625);
#3191=VECTOR('',#11245,0.65);
#3192=VECTOR('',#11250,0.635);
#3193=VECTOR('',#11259,0.41);
#3194=VECTOR('',#11262,0.4);
#3411=CIRCLE('',#9543,0.4);
#3412=CIRCLE('',#9544,0.3933);
#3413=CIRCLE('',#9546,0.4);
#3414=CIRCLE('',#9549,0.6);
#3415=CIRCLE('',#9551,0.65);
#3416=CIRCLE('',#9553,0.65);
#3417=CIRCLE('',#9555,0.62);
#3418=CIRCLE('',#9557,0.42);
#3419=CIRCLE('',#9559,0.3933);
#4085=VERTEX_POINT('',#28746);
#4086=VERTEX_POINT('',#28747);
#4087=VERTEX_POINT('',#28749);
#4088=VERTEX_POINT('',#28751);
#4089=VERTEX_POINT('',#28755);
#4090=VERTEX_POINT('',#28757);
#4091=VERTEX_POINT('',#28761);
#4092=VERTEX_POINT('',#28763);
#4093=VERTEX_POINT('',#28767);
#4094=VERTEX_POINT('',#28769);
#4095=VERTEX_POINT('',#28773);
#4096=VERTEX_POINT('',#28775);
#4097=VERTEX_POINT('',#28784);
#4098=VERTEX_POINT('',#28786);
#4099=VERTEX_POINT('',#28789);
#4100=VERTEX_POINT('',#28794);
#4101=VERTEX_POINT('',#28797);
#4102=VERTEX_POINT('',#28801);
#4103=VERTEX_POINT('',#28805);
#4104=VERTEX_POINT('',#28809);
#4105=VERTEX_POINT('',#28812);
#5233=EDGE_CURVE('',#4085,#4086,#2554,.T.);
#5234=EDGE_CURVE('',#4086,#4087,#2555,.T.);
#5235=EDGE_CURVE('',#4087,#4088,#2556,.T.);
#5236=EDGE_CURVE('',#4085,#4088,#2557,.T.);
#5237=EDGE_CURVE('',#4086,#4089,#2558,.T.);
#5238=EDGE_CURVE('',#4089,#4090,#2559,.T.);
#5239=EDGE_CURVE('',#4090,#4087,#2560,.T.);
#5240=EDGE_CURVE('',#4089,#4091,#2561,.T.);
#5241=EDGE_CURVE('',#4091,#4092,#2562,.T.);
#5242=EDGE_CURVE('',#4092,#4090,#2563,.T.);
#5243=EDGE_CURVE('',#4091,#4093,#2564,.T.);
#5244=EDGE_CURVE('',#4093,#4094,#2565,.T.);
#5245=EDGE_CURVE('',#4094,#4092,#2566,.T.);
#5246=EDGE_CURVE('',#4093,#4095,#2567,.T.);
#5247=EDGE_CURVE('',#4095,#4096,#2568,.T.);
#5248=EDGE_CURVE('',#4096,#4094,#2569,.T.);
#5249=EDGE_CURVE('',#4095,#4085,#2570,.T.);
#5250=EDGE_CURVE('',#4088,#4096,#2571,.T.);
#5251=EDGE_CURVE('',#4097,#4097,#3411,.T.);
#5252=EDGE_CURVE('',#4098,#4098,#3412,.T.);
#5253=EDGE_CURVE('',#4097,#4099,#2572,.T.);
#5254=EDGE_CURVE('',#4099,#4099,#3413,.T.);
#5255=EDGE_CURVE('',#4100,#4100,#3414,.T.);
#5256=EDGE_CURVE('',#4101,#4101,#3415,.T.);
#5257=EDGE_CURVE('',#4101,#4100,#2573,.T.);
#5258=EDGE_CURVE('',#4102,#4102,#3416,.T.);
#5259=EDGE_CURVE('',#4102,#4101,#2574,.T.);
#5260=EDGE_CURVE('',#4103,#4103,#3417,.T.);
#5261=EDGE_CURVE('',#4103,#4102,#2575,.T.);
#5262=EDGE_CURVE('',#4104,#4104,#3418,.T.);
#5263=EDGE_CURVE('',#4105,#4105,#3419,.F.);
#5264=EDGE_CURVE('',#4105,#4104,#2576,.T.);
#5265=EDGE_CURVE('',#4098,#4105,#2577,.T.);
#7439=ORIENTED_EDGE('',*,*,#5233,.T.);
#7440=ORIENTED_EDGE('',*,*,#5234,.T.);
#7441=ORIENTED_EDGE('',*,*,#5235,.T.);
#7442=ORIENTED_EDGE('',*,*,#5236,.F.);
#7443=ORIENTED_EDGE('',*,*,#5237,.T.);
#7444=ORIENTED_EDGE('',*,*,#5238,.T.);
#7445=ORIENTED_EDGE('',*,*,#5239,.T.);
#7446=ORIENTED_EDGE('',*,*,#5234,.F.);
#7447=ORIENTED_EDGE('',*,*,#5240,.T.);
#7448=ORIENTED_EDGE('',*,*,#5241,.T.);
#7449=ORIENTED_EDGE('',*,*,#5242,.T.);
#7450=ORIENTED_EDGE('',*,*,#5238,.F.);
#7451=ORIENTED_EDGE('',*,*,#5243,.T.);
#7452=ORIENTED_EDGE('',*,*,#5244,.T.);
#7453=ORIENTED_EDGE('',*,*,#5245,.T.);
#7454=ORIENTED_EDGE('',*,*,#5241,.F.);
#7455=ORIENTED_EDGE('',*,*,#5246,.T.);
#7456=ORIENTED_EDGE('',*,*,#5247,.T.);
#7457=ORIENTED_EDGE('',*,*,#5248,.T.);
#7458=ORIENTED_EDGE('',*,*,#5244,.F.);
#7459=ORIENTED_EDGE('',*,*,#5249,.T.);
#7460=ORIENTED_EDGE('',*,*,#5236,.T.);
#7461=ORIENTED_EDGE('',*,*,#5250,.T.);
#7462=ORIENTED_EDGE('',*,*,#5247,.F.);
#7463=ORIENTED_EDGE('',*,*,#5249,.F.);
#7464=ORIENTED_EDGE('',*,*,#5246,.F.);
#7465=ORIENTED_EDGE('',*,*,#5243,.F.);
#7466=ORIENTED_EDGE('',*,*,#5240,.F.);
#7467=ORIENTED_EDGE('',*,*,#5237,.F.);
#7468=ORIENTED_EDGE('',*,*,#5233,.F.);
#7469=ORIENTED_EDGE('',*,*,#5250,.F.);
#7470=ORIENTED_EDGE('',*,*,#5235,.F.);
#7471=ORIENTED_EDGE('',*,*,#5239,.F.);
#7472=ORIENTED_EDGE('',*,*,#5242,.F.);
#7473=ORIENTED_EDGE('',*,*,#5245,.F.);
#7474=ORIENTED_EDGE('',*,*,#5248,.F.);
#7475=ORIENTED_EDGE('',*,*,#5251,.T.);
#7476=ORIENTED_EDGE('',*,*,#5252,.F.);
#7477=ORIENTED_EDGE('',*,*,#5251,.F.);
#7478=ORIENTED_EDGE('',*,*,#5253,.T.);
#7479=ORIENTED_EDGE('',*,*,#5254,.T.);
#7480=ORIENTED_EDGE('',*,*,#5253,.F.);
#7481=ORIENTED_EDGE('',*,*,#5254,.F.);
#7482=ORIENTED_EDGE('',*,*,#5255,.F.);
#7483=ORIENTED_EDGE('',*,*,#5256,.F.);
#7484=ORIENTED_EDGE('',*,*,#5257,.T.);
#7485=ORIENTED_EDGE('',*,*,#5255,.T.);
#7486=ORIENTED_EDGE('',*,*,#5257,.F.);
#7487=ORIENTED_EDGE('',*,*,#5258,.F.);
#7488=ORIENTED_EDGE('',*,*,#5259,.T.);
#7489=ORIENTED_EDGE('',*,*,#5256,.T.);
#7490=ORIENTED_EDGE('',*,*,#5259,.F.);
#7491=ORIENTED_EDGE('',*,*,#5260,.F.);
#7492=ORIENTED_EDGE('',*,*,#5261,.T.);
#7493=ORIENTED_EDGE('',*,*,#5258,.T.);
#7494=ORIENTED_EDGE('',*,*,#5261,.F.);
#7495=ORIENTED_EDGE('',*,*,#5260,.T.);
#7496=ORIENTED_EDGE('',*,*,#5262,.F.);
#7497=ORIENTED_EDGE('',*,*,#5263,.F.);
#7498=ORIENTED_EDGE('',*,*,#5264,.T.);
#7499=ORIENTED_EDGE('',*,*,#5262,.T.);
#7500=ORIENTED_EDGE('',*,*,#5264,.F.);
#7501=ORIENTED_EDGE('',*,*,#5252,.T.);
#7502=ORIENTED_EDGE('',*,*,#5265,.T.);
#7503=ORIENTED_EDGE('',*,*,#5263,.T.);
#7504=ORIENTED_EDGE('',*,*,#5265,.F.);
#8235=CYLINDRICAL_SURFACE('',#9545,0.4);
#8236=CYLINDRICAL_SURFACE('',#9552,0.65);
#8237=CYLINDRICAL_SURFACE('',#9560,0.3933);
#8655=ADVANCED_FACE('',(#1418),#990,.F.);
#8656=ADVANCED_FACE('',(#1419),#991,.F.);
#8657=ADVANCED_FACE('',(#1420),#992,.F.);
#8658=ADVANCED_FACE('',(#1421),#993,.F.);
#8659=ADVANCED_FACE('',(#1422),#994,.F.);
#8660=ADVANCED_FACE('',(#1423),#995,.F.);
#8661=ADVANCED_FACE('',(#1424),#996,.F.);
#8662=ADVANCED_FACE('',(#1425),#997,.F.);
#8663=ADVANCED_FACE('',(#1426,#843),#998,.T.);
#8664=ADVANCED_FACE('',(#1427),#8235,.T.);
#8665=ADVANCED_FACE('',(#1428),#999,.F.);
#8666=ADVANCED_FACE('',(#1429),#1000,.T.);
#8667=ADVANCED_FACE('',(#1430),#198,.T.);
#8668=ADVANCED_FACE('',(#1431),#8236,.T.);
#8669=ADVANCED_FACE('',(#1432),#199,.T.);
#8670=ADVANCED_FACE('',(#1433,#844),#1001,.T.);
#8671=ADVANCED_FACE('',(#1434),#200,.T.);
#8672=ADVANCED_FACE('',(#1435),#8237,.T.);
#8792=CLOSED_SHELL('',(#8655,#8656,#8657,#8658,#8659,#8660,#8661,#8662));
#8793=CLOSED_SHELL('',(#8663,#8664,#8665,#8666,#8667,#8668,#8669,#8670,
#8671,#8672));
#9533=AXIS2_PLACEMENT_3D('',#28744,#11183,#11184);
#9534=AXIS2_PLACEMENT_3D('',#28745,#11185,#11186);
#9535=AXIS2_PLACEMENT_3D('',#28754,#11191,#11192);
#9536=AXIS2_PLACEMENT_3D('',#28760,#11196,#11197);
#9537=AXIS2_PLACEMENT_3D('',#28766,#11201,#11202);
#9538=AXIS2_PLACEMENT_3D('',#28772,#11206,#11207);
#9539=AXIS2_PLACEMENT_3D('',#28778,#11211,#11212);
#9540=AXIS2_PLACEMENT_3D('',#28781,#11215,#11216);
#9541=AXIS2_PLACEMENT_3D('',#28782,#11217,#11218);
#9542=AXIS2_PLACEMENT_3D('',#28783,#11219,#11220);
#9543=AXIS2_PLACEMENT_3D('',#28785,#11221,#11222);
#9544=AXIS2_PLACEMENT_3D('',#28787,#11223,#11224);
#9545=AXIS2_PLACEMENT_3D('',#28788,#11225,#11226);
#9546=AXIS2_PLACEMENT_3D('',#28791,#11228,#11229);
#9547=AXIS2_PLACEMENT_3D('',#28792,#11230,#11231);
#9548=AXIS2_PLACEMENT_3D('',#28793,#11232,#11233);
#9549=AXIS2_PLACEMENT_3D('',#28795,#11234,#11235);
#9550=AXIS2_PLACEMENT_3D('',#28796,#11236,#11237);
#9551=AXIS2_PLACEMENT_3D('',#28798,#11238,#11239);
#9552=AXIS2_PLACEMENT_3D('',#28800,#11241,#11242);
#9553=AXIS2_PLACEMENT_3D('',#28802,#11243,#11244);
#9554=AXIS2_PLACEMENT_3D('',#28804,#11246,#11247);
#9555=AXIS2_PLACEMENT_3D('',#28806,#11248,#11249);
#9556=AXIS2_PLACEMENT_3D('',#28808,#11251,#11252);
#9557=AXIS2_PLACEMENT_3D('',#28810,#11253,#11254);
#9558=AXIS2_PLACEMENT_3D('',#28811,#11255,#11256);
#9559=AXIS2_PLACEMENT_3D('',#28813,#11257,#11258);
#9560=AXIS2_PLACEMENT_3D('',#28815,#11260,#11261);
#11183=DIRECTION('axis',(0.,0.,1.));
#11184=DIRECTION('refdir',(1.,0.,0.));
#11185=DIRECTION('center_axis',(0.866025403784439,0.,-0.5));
#11186=DIRECTION('ref_axis',(0.5,0.,0.866025403784439));
#11187=DIRECTION('',(-0.5,0.,-0.866025403784439));
#11188=DIRECTION('',(0.,-1.,0.));
#11189=DIRECTION('',(0.5,0.,0.866025403784439));
#11190=DIRECTION('',(0.,-1.,0.));
#11191=DIRECTION('center_axis',(1.60246890531964E-16,0.,-1.));
#11192=DIRECTION('ref_axis',(1.,0.,1.60246890531964E-16));
#11193=DIRECTION('',(-1.,0.,-1.60246890531964E-16));
#11194=DIRECTION('',(0.,-1.,0.));
#11195=DIRECTION('',(1.,0.,1.60246890531964E-16));
#11196=DIRECTION('center_axis',(-0.866025403784439,0.,-0.5));
#11197=DIRECTION('ref_axis',(0.5,0.,-0.866025403784439));
#11198=DIRECTION('',(-0.5,0.,0.866025403784439));
#11199=DIRECTION('',(0.,-1.,0.));
#11200=DIRECTION('',(0.5,0.,-0.866025403784439));
#11201=DIRECTION('center_axis',(-0.866025403784439,0.,0.5));
#11202=DIRECTION('ref_axis',(-0.5,0.,-0.866025403784439));
#11203=DIRECTION('',(0.5,0.,0.866025403784439));
#11204=DIRECTION('',(0.,-1.,0.));
#11205=DIRECTION('',(-0.5,0.,-0.866025403784439));
#11206=DIRECTION('center_axis',(-1.60246890531964E-16,0.,1.));
#11207=DIRECTION('ref_axis',(-1.,0.,-1.60246890531964E-16));
#11208=DIRECTION('',(1.,0.,1.60246890531964E-16));
#11209=DIRECTION('',(0.,-1.,0.));
#11210=DIRECTION('',(-1.,0.,-1.60246890531964E-16));
#11211=DIRECTION('center_axis',(0.866025403784439,0.,0.5));
#11212=DIRECTION('ref_axis',(-0.5,0.,0.866025403784439));
#11213=DIRECTION('',(0.5,0.,-0.866025403784439));
#11214=DIRECTION('',(-0.5,0.,0.866025403784439));
#11215=DIRECTION('center_axis',(0.,1.,0.));
#11216=DIRECTION('ref_axis',(1.,0.,0.));
#11217=DIRECTION('center_axis',(0.,-1.,0.));
#11218=DIRECTION('ref_axis',(0.,0.,-1.));
#11219=DIRECTION('center_axis',(0.,1.,0.));
#11220=DIRECTION('ref_axis',(1.,0.,0.));
#11221=DIRECTION('center_axis',(0.,1.,0.));
#11222=DIRECTION('ref_axis',(1.,0.,0.));
#11223=DIRECTION('center_axis',(0.,1.,0.));
#11224=DIRECTION('ref_axis',(1.,0.,0.));
#11225=DIRECTION('center_axis',(0.,1.,0.));
#11226=DIRECTION('ref_axis',(1.,0.,0.));
#11227=DIRECTION('',(0.,-1.,0.));
#11228=DIRECTION('center_axis',(0.,1.,0.));
#11229=DIRECTION('ref_axis',(1.,0.,0.));
#11230=DIRECTION('center_axis',(0.,1.,0.));
#11231=DIRECTION('ref_axis',(1.,0.,0.));
#11232=DIRECTION('center_axis',(0.,1.,0.));
#11233=DIRECTION('ref_axis',(0.,0.,1.));
#11234=DIRECTION('center_axis',(0.,-1.,0.));
#11235=DIRECTION('ref_axis',(1.,0.,0.));
#11236=DIRECTION('center_axis',(0.,-1.,0.));
#11237=DIRECTION('ref_axis',(1.,0.,0.));
#11238=DIRECTION('center_axis',(0.,-1.,0.));
#11239=DIRECTION('ref_axis',(1.,0.,0.));
#11240=DIRECTION('',(0.707106781186548,0.707106781186547,8.65956056235493E-17));
#11241=DIRECTION('center_axis',(0.,-1.,0.));
#11242=DIRECTION('ref_axis',(1.,0.,0.));
#11243=DIRECTION('center_axis',(0.,-1.,0.));
#11244=DIRECTION('ref_axis',(1.,0.,0.));
#11245=DIRECTION('',(0.,1.,0.));
#11246=DIRECTION('center_axis',(0.,1.,0.));
#11247=DIRECTION('ref_axis',(1.,0.,0.));
#11248=DIRECTION('center_axis',(0.,-1.,0.));
#11249=DIRECTION('ref_axis',(1.,0.,0.));
#11250=DIRECTION('',(-0.707106781186548,0.707106781186547,-8.65956056235494E-17));
#11251=DIRECTION('center_axis',(0.,-1.,0.));
#11252=DIRECTION('ref_axis',(0.,0.,-1.));
#11253=DIRECTION('center_axis',(0.,-1.,0.));
#11254=DIRECTION('ref_axis',(1.,0.,0.));
#11255=DIRECTION('center_axis',(0.,1.,0.));
#11256=DIRECTION('ref_axis',(1.,0.,0.));
#11257=DIRECTION('center_axis',(0.,1.,0.));
#11258=DIRECTION('ref_axis',(1.,0.,0.));
#11259=DIRECTION('',(-0.447213595499958,0.894427190999916,-5.47678698264203E-17));
#11260=DIRECTION('center_axis',(0.,-1.,0.));
#11261=DIRECTION('ref_axis',(1.,0.,0.));
#11262=DIRECTION('',(0.,1.,0.));
#28744=CARTESIAN_POINT('',(0.,0.,0.));
#28745=CARTESIAN_POINT('Origin',(0.173205080756888,-0.8,-0.3));
#28746=CARTESIAN_POINT('',(0.346410161513775,-0.8,0.));
#28747=CARTESIAN_POINT('',(0.173205080756888,-0.8,-0.3));
#28748=CARTESIAN_POINT('',(0.346410161513775,-0.8,0.));
#28749=CARTESIAN_POINT('',(0.173205080756888,-1.28,-0.3));
#28750=CARTESIAN_POINT('',(0.173205080756888,-0.8,-0.3));
#28751=CARTESIAN_POINT('',(0.346410161513775,-1.28,0.));
#28752=CARTESIAN_POINT('',(0.346410161513775,-1.28,0.));
#28753=CARTESIAN_POINT('',(0.346410161513775,-0.8,0.));
#28754=CARTESIAN_POINT('Origin',(-0.173205080756888,-0.8,-0.3));
#28755=CARTESIAN_POINT('',(-0.173205080756888,-0.8,-0.3));
#28756=CARTESIAN_POINT('',(0.173205080756888,-0.8,-0.3));
#28757=CARTESIAN_POINT('',(-0.173205080756888,-1.28,-0.3));
#28758=CARTESIAN_POINT('',(-0.173205080756888,-0.8,-0.3));
#28759=CARTESIAN_POINT('',(0.173205080756888,-1.28,-0.3));
#28760=CARTESIAN_POINT('Origin',(-0.346410161513775,-0.8,-5.55111512312578E-17));
#28761=CARTESIAN_POINT('',(-0.346410161513775,-0.8,-4.24230095489963E-17));
#28762=CARTESIAN_POINT('',(-0.173205080756888,-0.8,-0.3));
#28763=CARTESIAN_POINT('',(-0.346410161513775,-1.28,-5.55111512312578E-17));
#28764=CARTESIAN_POINT('',(-0.346410161513775,-0.8,-4.24230095489963E-17));
#28765=CARTESIAN_POINT('',(-0.173205080756888,-1.28,-0.3));
#28766=CARTESIAN_POINT('Origin',(-0.173205080756888,-0.8,0.3));
#28767=CARTESIAN_POINT('',(-0.173205080756888,-0.8,0.3));
#28768=CARTESIAN_POINT('',(-0.346410161513775,-0.8,-4.24230095489963E-17));
#28769=CARTESIAN_POINT('',(-0.173205080756888,-1.28,0.3));
#28770=CARTESIAN_POINT('',(-0.173205080756888,-0.8,0.3));
#28771=CARTESIAN_POINT('',(-0.346410161513775,-1.28,-4.24230095489963E-17));
#28772=CARTESIAN_POINT('Origin',(0.173205080756888,-0.8,0.3));
#28773=CARTESIAN_POINT('',(0.173205080756888,-0.8,0.3));
#28774=CARTESIAN_POINT('',(-0.173205080756888,-0.8,0.3));
#28775=CARTESIAN_POINT('',(0.173205080756888,-1.28,0.3));
#28776=CARTESIAN_POINT('',(0.173205080756888,-0.8,0.3));
#28777=CARTESIAN_POINT('',(-0.173205080756888,-1.28,0.3));
#28778=CARTESIAN_POINT('Origin',(0.346410161513775,-0.8,0.));
#28779=CARTESIAN_POINT('',(0.173205080756888,-0.8,0.3));
#28780=CARTESIAN_POINT('',(0.173205080756888,-1.28,0.3));
#28781=CARTESIAN_POINT('Origin',(0.,-0.8,-5.55111512312578E-17));
#28782=CARTESIAN_POINT('Origin',(0.,-1.28,-5.55111512312578E-17));
#28783=CARTESIAN_POINT('Origin',(0.,-2.9,0.));
#28784=CARTESIAN_POINT('',(-0.4,-2.9,4.89858719658941E-17));
#28785=CARTESIAN_POINT('Origin',(0.,-2.9,0.));
#28786=CARTESIAN_POINT('',(-0.3933,-2.9,4.81653586104654E-17));
#28787=CARTESIAN_POINT('Origin',(0.,-2.9,0.));
#28788=CARTESIAN_POINT('Origin',(0.,-4.,0.));
#28789=CARTESIAN_POINT('',(-0.4,-4.,4.89858719658941E-17));
#28790=CARTESIAN_POINT('',(-0.4,-4.,4.89858719658941E-17));
#28791=CARTESIAN_POINT('Origin',(0.,-4.,0.));
#28792=CARTESIAN_POINT('Origin',(0.,-4.,0.));
#28793=CARTESIAN_POINT('Origin',(0.6,0.8,0.));
#28794=CARTESIAN_POINT('',(-0.6,0.8,-7.34788079488412E-17));
#28795=CARTESIAN_POINT('Origin',(0.,0.8,0.));
#28796=CARTESIAN_POINT('Origin',(0.,0.775,0.));
#28797=CARTESIAN_POINT('',(-0.65,0.75,-7.9602041944578E-17));
#28798=CARTESIAN_POINT('Origin',(0.,0.75,0.));
#28799=CARTESIAN_POINT('',(-0.625,0.775,-7.65404249467096E-17));
#28800=CARTESIAN_POINT('Origin',(0.,0.39,0.));
#28801=CARTESIAN_POINT('',(-0.65,0.0299999999999998,-7.9602041944578E-17));
#28802=CARTESIAN_POINT('Origin',(0.,0.0299999999999998,0.));
#28803=CARTESIAN_POINT('',(-0.65,0.39,-7.9602041944578E-17));
#28804=CARTESIAN_POINT('Origin',(0.,0.0150000000000001,0.));
#28805=CARTESIAN_POINT('',(-0.62,5.89805981832114E-17,-7.59281015471359E-17));
#28806=CARTESIAN_POINT('Origin',(0.,0.,0.));
#28807=CARTESIAN_POINT('',(-0.635,0.0150000000000001,-7.77650717458569E-17));
#28808=CARTESIAN_POINT('Origin',(0.42,0.,0.));
#28809=CARTESIAN_POINT('',(-0.42,-3.46944695195361E-18,-5.14351655641888E-17));
#28810=CARTESIAN_POINT('Origin',(0.,0.,0.));
#28811=CARTESIAN_POINT('Origin',(0.,-0.02,0.));
#28812=CARTESIAN_POINT('',(-0.3933,-0.0534000000000001,4.81653586104654E-17));
#28813=CARTESIAN_POINT('Origin',(0.,-0.0534000000000001,0.));
#28814=CARTESIAN_POINT('',(-0.41,-0.02,-5.02105187650415E-17));
#28815=CARTESIAN_POINT('Origin',(0.,-1.48,0.));
#28816=CARTESIAN_POINT('',(-0.3933,-1.48,-4.81653586104654E-17));
#34393=UNCERTAINTY_MEASURE_WITH_UNIT(LENGTH_MEASURE(0.001),#34434,
'DISTANCE_ACCURACY_VALUE',
'Maximum model space distance between geometric entities at asserted c
onnectivities');
#34404=UNCERTAINTY_MEASURE_WITH_UNIT(LENGTH_MEASURE(0.001),#34434,
'DISTANCE_ACCURACY_VALUE',
'Maximum model space distance between geometric entities at asserted c
onnectivities');
#34422=(
GEOMETRIC_REPRESENTATION_CONTEXT(3)
GLOBAL_UNCERTAINTY_ASSIGNED_CONTEXT((#34393))
GLOBAL_UNIT_ASSIGNED_CONTEXT((#34434,#34436,#34437))
REPRESENTATION_CONTEXT('','3D')
);
#34433=(
GEOMETRIC_REPRESENTATION_CONTEXT(3)
GLOBAL_UNCERTAINTY_ASSIGNED_CONTEXT((#34404))
GLOBAL_UNIT_ASSIGNED_CONTEXT((#34434,#34436,#34437))
REPRESENTATION_CONTEXT('','3D')
);
#34434=(
LENGTH_UNIT()
NAMED_UNIT(*)
SI_UNIT(.CENTI.,.METRE.)
);
#34436=(
NAMED_UNIT(*)
PLANE_ANGLE_UNIT()
SI_UNIT($,.RADIAN.)
);
#34437=(
NAMED_UNIT(*)
SI_UNIT($,.STERADIAN.)
SOLID_ANGLE_UNIT()
);
#34455=SHAPE_DEFINITION_REPRESENTATION(#34483,#34554);
#34483=PRODUCT_DEFINITION_SHAPE('',$,#34583);
#34554=SHAPE_REPRESENTATION('',(#9533),#34422);
#34565=PRODUCT_DEFINITION_CONTEXT('part definition',#34651,'design');
#34583=PRODUCT_DEFINITION('M8x40 clamp bolt','M8x40 clamp bolt',#34611,
#34565);
#34611=PRODUCT_DEFINITION_FORMATION('',$,#34670);
#34651=APPLICATION_CONTEXT(
'Core Data for Automotive Mechanical Design Process');
#34652=PRODUCT_CONTEXT('part definition',#34651,'mechanical');
#34670=PRODUCT('M8x40 clamp bolt','M8x40 clamp bolt','M8x40 clamp bolt',
(#34652));
#34744=COLOUR_RGB('Black',0.12,0.14,0.17);
#34745=FILL_AREA_STYLE_COLOUR('',#34744);
#34746=FILL_AREA_STYLE('',(#34745));
#34747=SURFACE_STYLE_FILL_AREA(#34746);
#34748=SURFACE_SIDE_STYLE('',(#34747));
#34749=SURFACE_STYLE_USAGE(.BOTH.,#34748);
#34750=PRESENTATION_STYLE_ASSIGNMENT((#34749));
ENDSEC;
END-ISO-10303-21;
